ISO-10303-21;
HEADER;
/* Generated by software containing ST-Developer
 * from STEP Tools, Inc. (www.steptools.com) 
 */

FILE_DESCRIPTION(
/* description */ ('Bin tilter linkage'),
/* implementation_level */ '2;1');

FILE_NAME(
/* name */ 'Screw and guide support (1).step',
/* time_stamp */ '2026-10-28T03:26:24-07:00',
/* author */ (''),
/* organization */ (''),
/* preprocessor_version */ 'ST-DEVELOPER v20.2',
/* originating_system */ 'Autodesk Translation Framework v15.17.0.0',
/* authorisation */ '');

FILE_SCHEMA (('AUTOMOTIVE_DESIGN { 1 0 10303 214 3 1 1 }'));
ENDSEC;

DATA;
#10=MECHANICAL_DESIGN_GEOMETRIC_PRESENTATION_REPRESENTATION('',(#882),#23728);
#670=SHAPE_REPRESENTATION_RELATIONSHIP('SRR','None',#24134,#776);
#776=ADVANCED_BREP_SHAPE_REPRESENTATION('',(#996),#23634);
#882=STYLED_ITEM('',(#24772),#996);
#996=MANIFOLD_SOLID_BREP('Body1',#12412);
#1203=FACE_BOUND('',#2956,.T.);
#1204=FACE_BOUND('',#2958,.T.);
#1205=FACE_BOUND('',#2959,.T.);
#1206=FACE_BOUND('',#2960,.T.);
#1207=FACE_BOUND('',#2961,.T.);
#1208=FACE_BOUND('',#2964,.T.);
#1209=FACE_BOUND('',#2968,.T.);
#1210=FACE_BOUND('',#2976,.T.);
#1211=FACE_BOUND('',#2977,.T.);
#1212=FACE_BOUND('',#2978,.T.);
#1213=FACE_BOUND('',#2979,.T.);
#1214=FACE_BOUND('',#2981,.T.);
#1215=FACE_BOUND('',#2983,.T.);
#1216=FACE_BOUND('',#2984,.T.);
#1577=PLANE('',#14045);
#1578=PLANE('',#14047);
#1579=PLANE('',#14054);
#1580=PLANE('',#14060);
#1581=PLANE('',#14070);
#1582=PLANE('',#14071);
#1583=PLANE('',#14072);
#1584=PLANE('',#14073);
#1585=PLANE('',#14074);
#2060=FACE_OUTER_BOUND('',#2953,.T.);
#2061=FACE_OUTER_BOUND('',#2954,.T.);
#2062=FACE_OUTER_BOUND('',#2955,.T.);
#2063=FACE_OUTER_BOUND('',#2957,.T.);
#2064=FACE_OUTER_BOUND('',#2962,.T.);
#2065=FACE_OUTER_BOUND('',#2963,.T.);
#2066=FACE_OUTER_BOUND('',#2965,.T.);
#2067=FACE_OUTER_BOUND('',#2966,.T.);
#2068=FACE_OUTER_BOUND('',#2967,.T.);
#2069=FACE_OUTER_BOUND('',#2969,.T.);
#2070=FACE_OUTER_BOUND('',#2970,.T.);
#2071=FACE_OUTER_BOUND('',#2971,.T.);
#2072=FACE_OUTER_BOUND('',#2972,.T.);
#2073=FACE_OUTER_BOUND('',#2973,.T.);
#2074=FACE_OUTER_BOUND('',#2974,.T.);
#2075=FACE_OUTER_BOUND('',#2975,.T.);
#2076=FACE_OUTER_BOUND('',#2980,.T.);
#2077=FACE_OUTER_BOUND('',#2982,.T.);
#2953=EDGE_LOOP('',(#9081,#9082,#9083,#9084));
#2954=EDGE_LOOP('',(#9085,#9086,#9087,#9088));
#2955=EDGE_LOOP('',(#9089,#9090,#9091,#9092));
#2956=EDGE_LOOP('',(#9093));
#2957=EDGE_LOOP('',(#9094,#9095,#9096,#9097,#9098,#9099));
#2958=EDGE_LOOP('',(#9100));
#2959=EDGE_LOOP('',(#9101));
#2960=EDGE_LOOP('',(#9102));
#2961=EDGE_LOOP('',(#9103));
#2962=EDGE_LOOP('',(#9104,#9105,#9106,#9107));
#2963=EDGE_LOOP('',(#9108));
#2964=EDGE_LOOP('',(#9109));
#2965=EDGE_LOOP('',(#9110,#9111,#9112,#9113));
#2966=EDGE_LOOP('',(#9114,#9115,#9116,#9117));
#2967=EDGE_LOOP('',(#9118));
#2968=EDGE_LOOP('',(#9119));
#2969=EDGE_LOOP('',(#9120,#9121,#9122,#9123));
#2970=EDGE_LOOP('',(#9124,#9125,#9126,#9127));
#2971=EDGE_LOOP('',(#9128,#9129,#9130,#9131));
#2972=EDGE_LOOP('',(#9132,#9133,#9134,#9135));
#2973=EDGE_LOOP('',(#9136,#9137,#9138,#9139));
#2974=EDGE_LOOP('',(#9140,#9141,#9142,#9143));
#2975=EDGE_LOOP('',(#9144,#9145,#9146,#9147,#9148,#9149));
#2976=EDGE_LOOP('',(#9150));
#2977=EDGE_LOOP('',(#9151));
#2978=EDGE_LOOP('',(#9152));
#2979=EDGE_LOOP('',(#9153));
#2980=EDGE_LOOP('',(#9154,#9155,#9156,#9157));
#2981=EDGE_LOOP('',(#9158));
#2982=EDGE_LOOP('',(#9159,#9160,#9161,#9162));
#2983=EDGE_LOOP('',(#9163));
#2984=EDGE_LOOP('',(#9164));
#4033=LINE('',#20533,#4708);
#4034=LINE('',#20536,#4709);
#4035=LINE('',#20541,#4710);
#4036=LINE('',#20545,#4711);
#4037=LINE('',#20547,#4712);
#4038=LINE('',#20548,#4713);
#4039=LINE('',#20553,#4714);
#4040=LINE('',#20555,#4715);
#4041=LINE('',#20557,#4716);
#4042=LINE('',#20558,#4717);
#4043=LINE('',#20569,#4718);
#4044=LINE('',#20577,#4719);
#4045=LINE('',#20581,#4720);
#4046=LINE('',#20588,#4721);
#4047=LINE('',#20592,#4722);
#4048=LINE('',#20596,#4723);
#4049=LINE('',#20600,#4724);
#4050=LINE('',#20603,#4725);
#4051=LINE('',#20605,#4726);
#4052=LINE('',#20606,#4727);
#4053=LINE('',#20609,#4728);
#4054=LINE('',#20610,#4729);
#4055=LINE('',#20612,#4730);
#4056=LINE('',#20613,#4731);
#4708=VECTOR('',#16388,1.);
#4709=VECTOR('',#16391,1.);
#4710=VECTOR('',#16396,0.165);
#4711=VECTOR('',#16401,1.);
#4712=VECTOR('',#16402,1.);
#4713=VECTOR('',#16403,1.);
#4714=VECTOR('',#16408,1.);
#4715=VECTOR('',#16409,1.);
#4716=VECTOR('',#16410,1.);
#4717=VECTOR('',#16411,1.);
#4718=VECTOR('',#16422,0.4);
#4719=VECTOR('',#16433,0.225);
#4720=VECTOR('',#16438,0.4);
#4721=VECTOR('',#16447,0.225);
#4722=VECTOR('',#16452,1.6);
#4723=VECTOR('',#16457,0.605);
#4724=VECTOR('',#16462,0.605);
#4725=VECTOR('',#16465,1.);
#4726=VECTOR('',#16466,1.);
#4727=VECTOR('',#16467,1.);
#4728=VECTOR('',#16470,1.);
#4729=VECTOR('',#16471,1.);
#4730=VECTOR('',#16474,1.);
#4731=VECTOR('',#16475,1.);
#5369=CIRCLE('',#14040,0.164999999999999);
#5370=CIRCLE('',#14041,0.164999999999999);
#5371=CIRCLE('',#14043,0.165);
#5372=CIRCLE('',#14044,0.165);
#5373=CIRCLE('',#14046,0.4);
#5374=CIRCLE('',#14048,0.605);
#5375=CIRCLE('',#14049,0.605);
#5376=CIRCLE('',#14050,1.6);
#5377=CIRCLE('',#14052,0.4);
#5378=CIRCLE('',#14053,0.4);
#5379=CIRCLE('',#14055,0.225);
#5380=CIRCLE('',#14057,0.225);
#5381=CIRCLE('',#14059,0.4);
#5382=CIRCLE('',#14061,0.225);
#5383=CIRCLE('',#14063,0.225);
#5384=CIRCLE('',#14065,1.6);
#5385=CIRCLE('',#14067,0.605);
#5386=CIRCLE('',#14069,0.605);
#6193=VERTEX_POINT('',#20529);
#6194=VERTEX_POINT('',#20530);
#6195=VERTEX_POINT('',#20532);
#6196=VERTEX_POINT('',#20534);
#6197=VERTEX_POINT('',#20538);
#6198=VERTEX_POINT('',#20540);
#6199=VERTEX_POINT('',#20544);
#6200=VERTEX_POINT('',#20546);
#6201=VERTEX_POINT('',#20549);
#6202=VERTEX_POINT('',#20552);
#6203=VERTEX_POINT('',#20554);
#6204=VERTEX_POINT('',#20556);
#6205=VERTEX_POINT('',#20559);
#6206=VERTEX_POINT('',#20561);
#6207=VERTEX_POINT('',#20563);
#6208=VERTEX_POINT('',#20566);
#6209=VERTEX_POINT('',#20568);
#6210=VERTEX_POINT('',#20572);
#6211=VERTEX_POINT('',#20575);
#6212=VERTEX_POINT('',#20579);
#6213=VERTEX_POINT('',#20583);
#6214=VERTEX_POINT('',#20586);
#6215=VERTEX_POINT('',#20590);
#6216=VERTEX_POINT('',#20594);
#6217=VERTEX_POINT('',#20598);
#6218=VERTEX_POINT('',#20602);
#6219=VERTEX_POINT('',#20604);
#6220=VERTEX_POINT('',#20608);
#7280=EDGE_CURVE('',#6193,#6194,#5369,.T.);
#7281=EDGE_CURVE('',#6195,#6193,#4033,.T.);
#7282=EDGE_CURVE('',#6196,#6195,#5370,.T.);
#7283=EDGE_CURVE('',#6194,#6196,#4034,.T.);
#7284=EDGE_CURVE('',#6197,#6197,#5371,.T.);
#7285=EDGE_CURVE('',#6197,#6198,#4035,.T.);
#7286=EDGE_CURVE('',#6198,#6198,#5372,.T.);
#7287=EDGE_CURVE('',#6193,#6199,#4036,.T.);
#7288=EDGE_CURVE('',#6199,#6200,#4037,.T.);
#7289=EDGE_CURVE('',#6200,#6195,#4038,.T.);
#7290=EDGE_CURVE('',#6201,#6201,#5373,.T.);
#7291=EDGE_CURVE('',#6202,#6200,#4039,.T.);
#7292=EDGE_CURVE('',#6202,#6203,#4040,.T.);
#7293=EDGE_CURVE('',#6203,#6204,#4041,.T.);
#7294=EDGE_CURVE('',#6196,#6204,#4042,.T.);
#7295=EDGE_CURVE('',#6205,#6205,#5374,.T.);
#7296=EDGE_CURVE('',#6206,#6206,#5375,.T.);
#7297=EDGE_CURVE('',#6207,#6207,#5376,.T.);
#7298=EDGE_CURVE('',#6208,#6208,#5377,.T.);
#7299=EDGE_CURVE('',#6208,#6209,#4043,.T.);
#7300=EDGE_CURVE('',#6209,#6209,#5378,.T.);
#7301=EDGE_CURVE('',#6210,#6210,#5379,.T.);
#7302=EDGE_CURVE('',#6211,#6211,#5380,.T.);
#7303=EDGE_CURVE('',#6211,#6210,#4044,.T.);
#7304=EDGE_CURVE('',#6212,#6212,#5381,.T.);
#7305=EDGE_CURVE('',#6212,#6201,#4045,.T.);
#7306=EDGE_CURVE('',#6213,#6213,#5382,.T.);
#7307=EDGE_CURVE('',#6214,#6214,#5383,.T.);
#7308=EDGE_CURVE('',#6214,#6213,#4046,.T.);
#7309=EDGE_CURVE('',#6215,#6215,#5384,.T.);
#7310=EDGE_CURVE('',#6215,#6207,#4047,.T.);
#7311=EDGE_CURVE('',#6216,#6216,#5385,.T.);
#7312=EDGE_CURVE('',#6216,#6206,#4048,.T.);
#7313=EDGE_CURVE('',#6217,#6217,#5386,.T.);
#7314=EDGE_CURVE('',#6217,#6205,#4049,.T.);
#7315=EDGE_CURVE('',#6203,#6218,#4050,.T.);
#7316=EDGE_CURVE('',#6218,#6219,#4051,.T.);
#7317=EDGE_CURVE('',#6204,#6219,#4052,.T.);
#7318=EDGE_CURVE('',#6220,#6202,#4053,.T.);
#7319=EDGE_CURVE('',#6220,#6199,#4054,.T.);
#7320=EDGE_CURVE('',#6219,#6194,#4055,.T.);
#7321=EDGE_CURVE('',#6218,#6220,#4056,.T.);
#9081=ORIENTED_EDGE('',*,*,#7280,.F.);
#9082=ORIENTED_EDGE('',*,*,#7281,.F.);
#9083=ORIENTED_EDGE('',*,*,#7282,.F.);
#9084=ORIENTED_EDGE('',*,*,#7283,.F.);
#9085=ORIENTED_EDGE('',*,*,#7284,.F.);
#9086=ORIENTED_EDGE('',*,*,#7285,.T.);
#9087=ORIENTED_EDGE('',*,*,#7286,.F.);
#9088=ORIENTED_EDGE('',*,*,#7285,.F.);
#9089=ORIENTED_EDGE('',*,*,#7281,.T.);
#9090=ORIENTED_EDGE('',*,*,#7287,.T.);
#9091=ORIENTED_EDGE('',*,*,#7288,.T.);
#9092=ORIENTED_EDGE('',*,*,#7289,.T.);
#9093=ORIENTED_EDGE('',*,*,#7290,.T.);
#9094=ORIENTED_EDGE('',*,*,#7282,.T.);
#9095=ORIENTED_EDGE('',*,*,#7289,.F.);
#9096=ORIENTED_EDGE('',*,*,#7291,.F.);
#9097=ORIENTED_EDGE('',*,*,#7292,.T.);
#9098=ORIENTED_EDGE('',*,*,#7293,.T.);
#9099=ORIENTED_EDGE('',*,*,#7294,.F.);
#9100=ORIENTED_EDGE('',*,*,#7295,.T.);
#9101=ORIENTED_EDGE('',*,*,#7296,.T.);
#9102=ORIENTED_EDGE('',*,*,#7297,.T.);
#9103=ORIENTED_EDGE('',*,*,#7286,.T.);
#9104=ORIENTED_EDGE('',*,*,#7298,.F.);
#9105=ORIENTED_EDGE('',*,*,#7299,.T.);
#9106=ORIENTED_EDGE('',*,*,#7300,.F.);
#9107=ORIENTED_EDGE('',*,*,#7299,.F.);
#9108=ORIENTED_EDGE('',*,*,#7298,.T.);
#9109=ORIENTED_EDGE('',*,*,#7301,.F.);
#9110=ORIENTED_EDGE('',*,*,#7302,.F.);
#9111=ORIENTED_EDGE('',*,*,#7303,.T.);
#9112=ORIENTED_EDGE('',*,*,#7301,.T.);
#9113=ORIENTED_EDGE('',*,*,#7303,.F.);
#9114=ORIENTED_EDGE('',*,*,#7304,.F.);
#9115=ORIENTED_EDGE('',*,*,#7305,.T.);
#9116=ORIENTED_EDGE('',*,*,#7290,.F.);
#9117=ORIENTED_EDGE('',*,*,#7305,.F.);
#9118=ORIENTED_EDGE('',*,*,#7304,.T.);
#9119=ORIENTED_EDGE('',*,*,#7306,.F.);
#9120=ORIENTED_EDGE('',*,*,#7307,.F.);
#9121=ORIENTED_EDGE('',*,*,#7308,.T.);
#9122=ORIENTED_EDGE('',*,*,#7306,.T.);
#9123=ORIENTED_EDGE('',*,*,#7308,.F.);
#9124=ORIENTED_EDGE('',*,*,#7309,.F.);
#9125=ORIENTED_EDGE('',*,*,#7310,.T.);
#9126=ORIENTED_EDGE('',*,*,#7297,.F.);
#9127=ORIENTED_EDGE('',*,*,#7310,.F.);
#9128=ORIENTED_EDGE('',*,*,#7311,.F.);
#9129=ORIENTED_EDGE('',*,*,#7312,.T.);
#9130=ORIENTED_EDGE('',*,*,#7296,.F.);
#9131=ORIENTED_EDGE('',*,*,#7312,.F.);
#9132=ORIENTED_EDGE('',*,*,#7313,.F.);
#9133=ORIENTED_EDGE('',*,*,#7314,.T.);
#9134=ORIENTED_EDGE('',*,*,#7295,.F.);
#9135=ORIENTED_EDGE('',*,*,#7314,.F.);
#9136=ORIENTED_EDGE('',*,*,#7315,.T.);
#9137=ORIENTED_EDGE('',*,*,#7316,.T.);
#9138=ORIENTED_EDGE('',*,*,#7317,.F.);
#9139=ORIENTED_EDGE('',*,*,#7293,.F.);
#9140=ORIENTED_EDGE('',*,*,#7318,.T.);
#9141=ORIENTED_EDGE('',*,*,#7291,.T.);
#9142=ORIENTED_EDGE('',*,*,#7288,.F.);
#9143=ORIENTED_EDGE('',*,*,#7319,.F.);
#9144=ORIENTED_EDGE('',*,*,#7280,.T.);
#9145=ORIENTED_EDGE('',*,*,#7320,.F.);
#9146=ORIENTED_EDGE('',*,*,#7316,.F.);
#9147=ORIENTED_EDGE('',*,*,#7321,.T.);
#9148=ORIENTED_EDGE('',*,*,#7319,.T.);
#9149=ORIENTED_EDGE('',*,*,#7287,.F.);
#9150=ORIENTED_EDGE('',*,*,#7284,.T.);
#9151=ORIENTED_EDGE('',*,*,#7309,.T.);
#9152=ORIENTED_EDGE('',*,*,#7311,.T.);
#9153=ORIENTED_EDGE('',*,*,#7313,.T.);
#9154=ORIENTED_EDGE('',*,*,#7283,.T.);
#9155=ORIENTED_EDGE('',*,*,#7294,.T.);
#9156=ORIENTED_EDGE('',*,*,#7317,.T.);
#9157=ORIENTED_EDGE('',*,*,#7320,.T.);
#9158=ORIENTED_EDGE('',*,*,#7300,.T.);
#9159=ORIENTED_EDGE('',*,*,#7321,.F.);
#9160=ORIENTED_EDGE('',*,*,#7315,.F.);
#9161=ORIENTED_EDGE('',*,*,#7292,.F.);
#9162=ORIENTED_EDGE('',*,*,#7318,.F.);
#9163=ORIENTED_EDGE('',*,*,#7302,.T.);
#9164=ORIENTED_EDGE('',*,*,#7307,.T.);
#11352=CYLINDRICAL_SURFACE('',#14039,0.164999999999999);
#11353=CYLINDRICAL_SURFACE('',#14042,0.165);
#11354=CYLINDRICAL_SURFACE('',#14051,0.4);
#11355=CYLINDRICAL_SURFACE('',#14056,0.225);
#11356=CYLINDRICAL_SURFACE('',#14058,0.4);
#11357=CYLINDRICAL_SURFACE('',#14062,0.225);
#11358=CYLINDRICAL_SURFACE('',#14064,1.6);
#11359=CYLINDRICAL_SURFACE('',#14066,0.605);
#11360=CYLINDRICAL_SURFACE('',#14068,0.605);
#11785=ADVANCED_FACE('',(#2060),#11352,.F.);
#11786=ADVANCED_FACE('',(#2061),#11353,.F.);
#11787=ADVANCED_FACE('',(#2062,#1203),#1577,.T.);
#11788=ADVANCED_FACE('',(#2063,#1204,#1205,#1206,#1207),#1578,.T.);
#11789=ADVANCED_FACE('',(#2064),#11354,.F.);
#11790=ADVANCED_FACE('',(#2065,#1208),#1579,.T.);
#11791=ADVANCED_FACE('',(#2066),#11355,.F.);
#11792=ADVANCED_FACE('',(#2067),#11356,.F.);
#11793=ADVANCED_FACE('',(#2068,#1209),#1580,.T.);
#11794=ADVANCED_FACE('',(#2069),#11357,.F.);
#11795=ADVANCED_FACE('',(#2070),#11358,.F.);
#11796=ADVANCED_FACE('',(#2071),#11359,.F.);
#11797=ADVANCED_FACE('',(#2072),#11360,.F.);
#11798=ADVANCED_FACE('',(#2073),#1581,.T.);
#11799=ADVANCED_FACE('',(#2074),#1582,.T.);
#11800=ADVANCED_FACE('',(#2075,#1210,#1211,#1212,#1213),#1583,.T.);
#11801=ADVANCED_FACE('',(#2076,#1214),#1584,.T.);
#11802=ADVANCED_FACE('',(#2077,#1215,#1216),#1585,.F.);
#12412=CLOSED_SHELL('',(#11785,#11786,#11787,#11788,#11789,#11790,#11791,
#11792,#11793,#11794,#11795,#11796,#11797,#11798,#11799,#11800,#11801,#11802));
#14038=AXIS2_PLACEMENT_3D('',#20527,#16382,#16383);
#14039=AXIS2_PLACEMENT_3D('',#20528,#16384,#16385);
#14040=AXIS2_PLACEMENT_3D('',#20531,#16386,#16387);
#14041=AXIS2_PLACEMENT_3D('',#20535,#16389,#16390);
#14042=AXIS2_PLACEMENT_3D('',#20537,#16392,#16393);
#14043=AXIS2_PLACEMENT_3D('',#20539,#16394,#16395);
#14044=AXIS2_PLACEMENT_3D('',#20542,#16397,#16398);
#14045=AXIS2_PLACEMENT_3D('',#20543,#16399,#16400);
#14046=AXIS2_PLACEMENT_3D('',#20550,#16404,#16405);
#14047=AXIS2_PLACEMENT_3D('',#20551,#16406,#16407);
#14048=AXIS2_PLACEMENT_3D('',#20560,#16412,#16413);
#14049=AXIS2_PLACEMENT_3D('',#20562,#16414,#16415);
#14050=AXIS2_PLACEMENT_3D('',#20564,#16416,#16417);
#14051=AXIS2_PLACEMENT_3D('',#20565,#16418,#16419);
#14052=AXIS2_PLACEMENT_3D('',#20567,#16420,#16421);
#14053=AXIS2_PLACEMENT_3D('',#20570,#16423,#16424);
#14054=AXIS2_PLACEMENT_3D('',#20571,#16425,#16426);
#14055=AXIS2_PLACEMENT_3D('',#20573,#16427,#16428);
#14056=AXIS2_PLACEMENT_3D('',#20574,#16429,#16430);
#14057=AXIS2_PLACEMENT_3D('',#20576,#16431,#16432);
#14058=AXIS2_PLACEMENT_3D('',#20578,#16434,#16435);
#14059=AXIS2_PLACEMENT_3D('',#20580,#16436,#16437);
#14060=AXIS2_PLACEMENT_3D('',#20582,#16439,#16440);
#14061=AXIS2_PLACEMENT_3D('',#20584,#16441,#16442);
#14062=AXIS2_PLACEMENT_3D('',#20585,#16443,#16444);
#14063=AXIS2_PLACEMENT_3D('',#20587,#16445,#16446);
#14064=AXIS2_PLACEMENT_3D('',#20589,#16448,#16449);
#14065=AXIS2_PLACEMENT_3D('',#20591,#16450,#16451);
#14066=AXIS2_PLACEMENT_3D('',#20593,#16453,#16454);
#14067=AXIS2_PLACEMENT_3D('',#20595,#16455,#16456);
#14068=AXIS2_PLACEMENT_3D('',#20597,#16458,#16459);
#14069=AXIS2_PLACEMENT_3D('',#20599,#16460,#16461);
#14070=AXIS2_PLACEMENT_3D('',#20601,#16463,#16464);
#14071=AXIS2_PLACEMENT_3D('',#20607,#16468,#16469);
#14072=AXIS2_PLACEMENT_3D('',#20611,#16472,#16473);
#14073=AXIS2_PLACEMENT_3D('',#20614,#16476,#16477);
#14074=AXIS2_PLACEMENT_3D('',#20615,#16478,#16479);
#16382=DIRECTION('axis',(0.,0.,1.));
#16383=DIRECTION('refdir',(1.,0.,0.));
#16384=DIRECTION('center_axis',(1.,0.,0.));
#16385=DIRECTION('ref_axis',(0.,0.,-1.));
#16386=DIRECTION('center_axis',(1.,0.,0.));
#16387=DIRECTION('ref_axis',(0.,0.,-1.));
#16388=DIRECTION('',(-1.,0.,0.));
#16389=DIRECTION('center_axis',(-1.,0.,0.));
#16390=DIRECTION('ref_axis',(0.,0.,-1.));
#16391=DIRECTION('',(1.,0.,0.));
#16392=DIRECTION('center_axis',(1.,0.,0.));
#16393=DIRECTION('ref_axis',(0.,0.,-1.));
#16394=DIRECTION('center_axis',(1.,0.,0.));
#16395=DIRECTION('ref_axis',(0.,0.,-1.));
#16396=DIRECTION('',(1.,0.,0.));
#16397=DIRECTION('center_axis',(-1.,0.,0.));
#16398=DIRECTION('ref_axis',(0.,0.,-1.));
#16399=DIRECTION('center_axis',(0.,0.,1.));
#16400=DIRECTION('ref_axis',(1.,0.,0.));
#16401=DIRECTION('',(0.,-1.,0.));
#16402=DIRECTION('',(1.,0.,0.));
#16403=DIRECTION('',(0.,1.,0.));
#16404=DIRECTION('center_axis',(0.,0.,-1.));
#16405=DIRECTION('ref_axis',(1.,0.,0.));
#16406=DIRECTION('center_axis',(1.,0.,0.));
#16407=DIRECTION('ref_axis',(0.,1.,0.));
#16408=DIRECTION('',(0.,0.,1.));
#16409=DIRECTION('',(0.,1.,0.));
#16410=DIRECTION('',(0.,0.,1.));
#16411=DIRECTION('',(0.,1.,0.));
#16412=DIRECTION('center_axis',(-1.,0.,0.));
#16413=DIRECTION('ref_axis',(0.,0.,-1.));
#16414=DIRECTION('center_axis',(-1.,0.,0.));
#16415=DIRECTION('ref_axis',(0.,0.,-1.));
#16416=DIRECTION('center_axis',(-1.,0.,0.));
#16417=DIRECTION('ref_axis',(0.,0.,-1.));
#16418=DIRECTION('center_axis',(0.,0.,1.));
#16419=DIRECTION('ref_axis',(1.,0.,0.));
#16420=DIRECTION('center_axis',(0.,0.,1.));
#16421=DIRECTION('ref_axis',(1.,0.,0.));
#16422=DIRECTION('',(0.,0.,1.));
#16423=DIRECTION('center_axis',(0.,0.,-1.));
#16424=DIRECTION('ref_axis',(1.,0.,0.));
#16425=DIRECTION('center_axis',(0.,0.,1.));
#16426=DIRECTION('ref_axis',(1.,0.,0.));
#16427=DIRECTION('center_axis',(0.,0.,1.));
#16428=DIRECTION('ref_axis',(1.,0.,0.));
#16429=DIRECTION('center_axis',(0.,0.,1.));
#16430=DIRECTION('ref_axis',(1.,0.,0.));
#16431=DIRECTION('center_axis',(0.,0.,1.));
#16432=DIRECTION('ref_axis',(1.,0.,0.));
#16433=DIRECTION('',(0.,0.,1.));
#16434=DIRECTION('center_axis',(0.,0.,1.));
#16435=DIRECTION('ref_axis',(1.,0.,0.));
#16436=DIRECTION('center_axis',(0.,0.,1.));
#16437=DIRECTION('ref_axis',(1.,0.,0.));
#16438=DIRECTION('',(0.,0.,1.));
#16439=DIRECTION('center_axis',(0.,0.,1.));
#16440=DIRECTION('ref_axis',(1.,0.,0.));
#16441=DIRECTION('center_axis',(0.,0.,1.));
#16442=DIRECTION('ref_axis',(1.,0.,0.));
#16443=DIRECTION('center_axis',(0.,0.,1.));
#16444=DIRECTION('ref_axis',(1.,0.,0.));
#16445=DIRECTION('center_axis',(0.,0.,1.));
#16446=DIRECTION('ref_axis',(1.,0.,0.));
#16447=DIRECTION('',(0.,0.,1.));
#16448=DIRECTION('center_axis',(1.,0.,0.));
#16449=DIRECTION('ref_axis',(0.,0.,-1.));
#16450=DIRECTION('center_axis',(1.,0.,0.));
#16451=DIRECTION('ref_axis',(0.,0.,-1.));
#16452=DIRECTION('',(1.,0.,0.));
#16453=DIRECTION('center_axis',(1.,0.,0.));
#16454=DIRECTION('ref_axis',(0.,0.,-1.));
#16455=DIRECTION('center_axis',(1.,0.,0.));
#16456=DIRECTION('ref_axis',(0.,0.,-1.));
#16457=DIRECTION('',(1.,0.,0.));
#16458=DIRECTION('center_axis',(1.,0.,0.));
#16459=DIRECTION('ref_axis',(0.,0.,-1.));
#16460=DIRECTION('center_axis',(1.,0.,0.));
#16461=DIRECTION('ref_axis',(0.,0.,-1.));
#16462=DIRECTION('',(1.,0.,0.));
#16463=DIRECTION('center_axis',(0.,1.,0.));
#16464=DIRECTION('ref_axis',(-1.,0.,0.));
#16465=DIRECTION('',(-1.,0.,0.));
#16466=DIRECTION('',(0.,0.,1.));
#16467=DIRECTION('',(-1.,0.,0.));
#16468=DIRECTION('center_axis',(0.,-1.,0.));
#16469=DIRECTION('ref_axis',(1.,0.,0.));
#16470=DIRECTION('',(1.,0.,0.));
#16471=DIRECTION('',(0.,0.,1.));
#16472=DIRECTION('center_axis',(-1.,0.,0.));
#16473=DIRECTION('ref_axis',(0.,-1.,0.));
#16474=DIRECTION('',(0.,-1.,0.));
#16475=DIRECTION('',(0.,-1.,0.));
#16476=DIRECTION('center_axis',(0.,0.,1.));
#16477=DIRECTION('ref_axis',(1.,0.,0.));
#16478=DIRECTION('center_axis',(0.,0.,1.));
#16479=DIRECTION('ref_axis',(1.,0.,0.));
#20527=CARTESIAN_POINT('',(0.,0.,0.));
#20528=CARTESIAN_POINT('Origin',(-0.1,-4.5,9.85));
#20529=CARTESIAN_POINT('',(0.,-4.56873863542434,10.));
#20530=CARTESIAN_POINT('',(0.,-4.43126136457566,10.));
#20531=CARTESIAN_POINT('Origin',(0.,-4.5,9.85));
#20532=CARTESIAN_POINT('',(1.,-4.56873863542434,10.));
#20533=CARTESIAN_POINT('',(-0.1,-4.56873863542434,10.));
#20534=CARTESIAN_POINT('',(1.,-4.43126136457566,10.));
#20535=CARTESIAN_POINT('Origin',(1.,-4.5,9.85));
#20536=CARTESIAN_POINT('',(-0.1,-4.43126136457566,10.));
#20537=CARTESIAN_POINT('Origin',(-0.1,-4.5,6.15));
#20538=CARTESIAN_POINT('',(0.,-4.5,6.315));
#20539=CARTESIAN_POINT('Origin',(0.,-4.5,6.15));
#20540=CARTESIAN_POINT('',(1.,-4.5,6.315));
#20541=CARTESIAN_POINT('',(-0.1,-4.5,6.315));
#20542=CARTESIAN_POINT('Origin',(1.,-4.5,6.15));
#20543=CARTESIAN_POINT('Origin',(0.5,-4.5,10.));
#20544=CARTESIAN_POINT('',(0.,-9.,10.));
#20545=CARTESIAN_POINT('',(0.,0.,10.));
#20546=CARTESIAN_POINT('',(1.,-9.,10.));
#20547=CARTESIAN_POINT('',(0.,-9.,10.));
#20548=CARTESIAN_POINT('',(1.,-9.,10.));
#20549=CARTESIAN_POINT('',(0.1,-8.2,10.));
#20550=CARTESIAN_POINT('Origin',(0.5,-8.2,10.));
#20551=CARTESIAN_POINT('Origin',(1.,-9.,1.));
#20552=CARTESIAN_POINT('',(1.,-9.,1.));
#20553=CARTESIAN_POINT('',(1.,-9.,1.));
#20554=CARTESIAN_POINT('',(1.,0.,1.));
#20555=CARTESIAN_POINT('',(1.,-9.,1.));
#20556=CARTESIAN_POINT('',(1.,0.,10.));
#20557=CARTESIAN_POINT('',(1.,0.,1.));
#20558=CARTESIAN_POINT('',(1.,-9.,10.));
#20559=CARTESIAN_POINT('',(1.,-2.,8.605));
#20560=CARTESIAN_POINT('Origin',(1.,-2.,8.));
#20561=CARTESIAN_POINT('',(1.,-7.,8.605));
#20562=CARTESIAN_POINT('Origin',(1.,-7.,8.));
#20563=CARTESIAN_POINT('',(1.,-4.5,9.6));
#20564=CARTESIAN_POINT('Origin',(1.,-4.5,8.));
#20565=CARTESIAN_POINT('Origin',(0.5,-0.8,1.8));
#20566=CARTESIAN_POINT('',(0.1,-0.8,1.8));
#20567=CARTESIAN_POINT('Origin',(0.5,-0.8,1.8));
#20568=CARTESIAN_POINT('',(0.1,-0.8,10.));
#20569=CARTESIAN_POINT('',(0.1,-0.8,1.8));
#20570=CARTESIAN_POINT('Origin',(0.5,-0.8,10.));
#20571=CARTESIAN_POINT('Origin',(0.5,-0.8,1.8));
#20572=CARTESIAN_POINT('',(0.275,-0.8,1.8));
#20573=CARTESIAN_POINT('Origin',(0.5,-0.8,1.8));
#20574=CARTESIAN_POINT('Origin',(0.5,-0.8,0.9));
#20575=CARTESIAN_POINT('',(0.275,-0.8,1.));
#20576=CARTESIAN_POINT('Origin',(0.5,-0.8,1.));
#20577=CARTESIAN_POINT('',(0.275,-0.8,0.9));
#20578=CARTESIAN_POINT('Origin',(0.5,-8.2,1.8));
#20579=CARTESIAN_POINT('',(0.1,-8.2,1.8));
#20580=CARTESIAN_POINT('Origin',(0.5,-8.2,1.8));
#20581=CARTESIAN_POINT('',(0.1,-8.2,1.8));
#20582=CARTESIAN_POINT('Origin',(0.5,-8.2,1.8));
#20583=CARTESIAN_POINT('',(0.275,-8.2,1.8));
#20584=CARTESIAN_POINT('Origin',(0.5,-8.2,1.8));
#20585=CARTESIAN_POINT('Origin',(0.5,-8.2,0.9));
#20586=CARTESIAN_POINT('',(0.275,-8.2,1.));
#20587=CARTESIAN_POINT('Origin',(0.5,-8.2,1.));
#20588=CARTESIAN_POINT('',(0.275,-8.2,0.9));
#20589=CARTESIAN_POINT('Origin',(-0.1,-4.5,8.));
#20590=CARTESIAN_POINT('',(0.,-4.5,9.6));
#20591=CARTESIAN_POINT('Origin',(0.,-4.5,8.));
#20592=CARTESIAN_POINT('',(-0.1,-4.5,9.6));
#20593=CARTESIAN_POINT('Origin',(-0.1,-7.,8.));
#20594=CARTESIAN_POINT('',(0.,-7.,8.605));
#20595=CARTESIAN_POINT('Origin',(0.,-7.,8.));
#20596=CARTESIAN_POINT('',(-0.1,-7.,8.605));
#20597=CARTESIAN_POINT('Origin',(-0.1,-2.,8.));
#20598=CARTESIAN_POINT('',(0.,-2.,8.605));
#20599=CARTESIAN_POINT('Origin',(0.,-2.,8.));
#20600=CARTESIAN_POINT('',(-0.1,-2.,8.605));
#20601=CARTESIAN_POINT('Origin',(1.,0.,1.));
#20602=CARTESIAN_POINT('',(0.,0.,1.));
#20603=CARTESIAN_POINT('',(1.,0.,1.));
#20604=CARTESIAN_POINT('',(0.,0.,10.));
#20605=CARTESIAN_POINT('',(0.,0.,1.));
#20606=CARTESIAN_POINT('',(1.,0.,10.));
#20607=CARTESIAN_POINT('Origin',(0.,-9.,1.));
#20608=CARTESIAN_POINT('',(0.,-9.,1.));
#20609=CARTESIAN_POINT('',(0.,-9.,1.));
#20610=CARTESIAN_POINT('',(0.,-9.,1.));
#20611=CARTESIAN_POINT('Origin',(0.,0.,1.));
#20612=CARTESIAN_POINT('',(0.,0.,10.));
#20613=CARTESIAN_POINT('',(0.,0.,1.));
#20614=CARTESIAN_POINT('Origin',(0.5,-4.5,10.));
#20615=CARTESIAN_POINT('Origin',(0.5,-4.5,1.));
#23517=UNCERTAINTY_MEASURE_WITH_UNIT(LENGTH_MEASURE(0.001),#23729,
'DISTANCE_ACCURACY_VALUE',
'Maximum model space distance between geometric entities at asserted c
onnectivities');
#23611=UNCERTAINTY_MEASURE_WITH_UNIT(LENGTH_MEASURE(0.001),#23729,
'DISTANCE_ACCURACY_VALUE',
'Maximum model space distance between geometric entities at asserted c
onnectivities');
#23634=(
GEOMETRIC_REPRESENTATION_CONTEXT(3)
GLOBAL_UNCERTAINTY_ASSIGNED_CONTEXT((#23517))
GLOBAL_UNIT_ASSIGNED_CONTEXT((#23729,#23731,#23732))
REPRESENTATION_CONTEXT('','3D')
);
#23728=(
GEOMETRIC_REPRESENTATION_CONTEXT(3)
GLOBAL_UNCERTAINTY_ASSIGNED_CONTEXT((#23611))
GLOBAL_UNIT_ASSIGNED_CONTEXT((#23729,#23731,#23732))
REPRESENTATION_CONTEXT('','3D')
);
#23729=(
LENGTH_UNIT()
NAMED_UNIT(*)
SI_UNIT(.CENTI.,.METRE.)
);
#23731=(
NAMED_UNIT(*)
PLANE_ANGLE_UNIT()
SI_UNIT($,.RADIAN.)
);
#23732=(
NAMED_UNIT(*)
SI_UNIT($,.STERADIAN.)
SOLID_ANGLE_UNIT()
);
#23755=SHAPE_DEFINITION_REPRESENTATION(#23871,#24134);
#23871=PRODUCT_DEFINITION_SHAPE('',$,#24251);
#24134=SHAPE_REPRESENTATION('',(#14038),#23634);
#24228=PRODUCT_DEFINITION_CONTEXT('part definition',#24578,'design');
#24251=PRODUCT_DEFINITION('Screw and guide support (1)',
'Screw and guide support (1)',#24367,#24228);
#24367=PRODUCT_DEFINITION_FORMATION('',$,#24602);
#24578=APPLICATION_CONTEXT(
'Core Data for Automotive Mechanical Design Process');
#24579=PRODUCT_CONTEXT('part definition',#24578,'mechanical');
#24602=PRODUCT('Screw and guide support (1)',
'Screw and guide support (1)','Screw and guide support (1)',(#24579));
#24766=COLOUR_RGB('Black',0.12,0.14,0.17);
#24767=FILL_AREA_STYLE_COLOUR('',#24766);
#24768=FILL_AREA_STYLE('',(#24767));
#24769=SURFACE_STYLE_FILL_AREA(#24768);
#24770=SURFACE_SIDE_STYLE('',(#24769));
#24771=SURFACE_STYLE_USAGE(.BOTH.,#24770);
#24772=PRESENTATION_STYLE_ASSIGNMENT((#24771));
ENDSEC;
END-ISO-10303-21;
